ISO-10303-21;
HEADER;
/* Generated by software containing ST-Developer
 * from STEP Tools, Inc. (www.steptools.com) 
 */

FILE_DESCRIPTION(
/* description */ (''),
/* implementation_level */ '2;1');

FILE_NAME(
/* name */ 'Rail_01.step',
/* time_stamp */ '2026-10-19T01:17:59+06:00',
/* author */ (''),
/* organization */ (''),
/* preprocessor_version */ 'ST-DEVELOPER v20.2',
/* originating_system */ 'Autodesk Translation Framework v15.15.0.0',
/* authorisation */ '');

FILE_SCHEMA (('AUTOMOTIVE_DESIGN { 1 0 10303 214 3 1 1 }'));
ENDSEC;

DATA;
#10=MECHANICAL_DESIGN_GEOMETRIC_PRESENTATION_REPRESENTATION('',(#754),#48369);
#623=SHAPE_REPRESENTATION_RELATIONSHIP('SRR','None',#48423,#634);
#634=ADVANCED_BREP_SHAPE_REPRESENTATION('',(#780),#48368);
#754=STYLED_ITEM('',(#48510),#780);
#780=MANIFOLD_SOLID_BREP('Rail_01',#20133);
#1189=CYLINDRICAL_SURFACE('',#21841,0.450000000000145);
#1190=CYLINDRICAL_SURFACE('',#21844,2.46743797397102);
#1191=CYLINDRICAL_SURFACE('',#21847,0.725000000000007);
#1192=CYLINDRICAL_SURFACE('',#21851,0.599999999999981);
#1193=CYLINDRICAL_SURFACE('',#21854,2.3640229247478);
#1194=CYLINDRICAL_SURFACE('',#21857,1.39999999999995);
#1195=CYLINDRICAL_SURFACE('',#21861,1.05000000000001);
#1196=CYLINDRICAL_SURFACE('',#21865,1.04999999999996);
#1197=CYLINDRICAL_SURFACE('',#21869,1.09999999999999);
#1198=CYLINDRICAL_SURFACE('',#21885,0.450000000000145);
#1199=CYLINDRICAL_SURFACE('',#21887,2.46743797397102);
#1200=CYLINDRICAL_SURFACE('',#21889,0.725000000000007);
#1201=CYLINDRICAL_SURFACE('',#21892,0.599999999999981);
#1202=CYLINDRICAL_SURFACE('',#21894,2.3640229247478);
#1203=CYLINDRICAL_SURFACE('',#21896,1.39999999999995);
#1204=CYLINDRICAL_SURFACE('',#21899,1.05000000000001);
#1205=CYLINDRICAL_SURFACE('',#21902,1.04999999999996);
#1206=CYLINDRICAL_SURFACE('',#21905,1.09999999999999);
#2215=FACE_OUTER_BOUND('',#3353,.T.);
#2216=FACE_OUTER_BOUND('',#3354,.T.);
#2217=FACE_OUTER_BOUND('',#3355,.T.);
#2218=FACE_OUTER_BOUND('',#3356,.T.);
#2219=FACE_OUTER_BOUND('',#3357,.T.);
#2220=FACE_OUTER_BOUND('',#3358,.T.);
#2221=FACE_OUTER_BOUND('',#3359,.T.);
#2222=FACE_OUTER_BOUND('',#3360,.T.);
#2223=FACE_OUTER_BOUND('',#3361,.T.);
#2224=FACE_OUTER_BOUND('',#3362,.T.);
#2225=FACE_OUTER_BOUND('',#3363,.T.);
#2226=FACE_OUTER_BOUND('',#3364,.T.);
#2227=FACE_OUTER_BOUND('',#3365,.T.);
#2228=FACE_OUTER_BOUND('',#3366,.T.);
#2229=FACE_OUTER_BOUND('',#3367,.T.);
#2230=FACE_OUTER_BOUND('',#3368,.T.);
#2231=FACE_OUTER_BOUND('',#3369,.T.);
#2232=FACE_OUTER_BOUND('',#3370,.T.);
#2233=FACE_OUTER_BOUND('',#3371,.T.);
#2234=FACE_OUTER_BOUND('',#3372,.T.);
#2235=FACE_OUTER_BOUND('',#3373,.T.);
#2236=FACE_OUTER_BOUND('',#3374,.T.);
#2237=FACE_OUTER_BOUND('',#3375,.T.);
#2238=FACE_OUTER_BOUND('',#3376,.T.);
#2239=FACE_OUTER_BOUND('',#3377,.T.);
#2240=FACE_OUTER_BOUND('',#3378,.T.);
#2241=FACE_OUTER_BOUND('',#3379,.T.);
#2242=FACE_OUTER_BOUND('',#3380,.T.);
#2243=FACE_OUTER_BOUND('',#3381,.T.);
#2244=FACE_OUTER_BOUND('',#3382,.T.);
#2245=FACE_OUTER_BOUND('',#3383,.T.);
#2246=FACE_OUTER_BOUND('',#3384,.T.);
#2247=FACE_OUTER_BOUND('',#3385,.T.);
#2248=FACE_OUTER_BOUND('',#3386,.T.);
#2249=FACE_OUTER_BOUND('',#3387,.T.);
#2250=FACE_OUTER_BOUND('',#3388,.T.);
#3353=EDGE_LOOP('',(#18331,#18332,#18333,#18334));
#3354=EDGE_LOOP('',(#18335,#18336,#18337,#18338));
#3355=EDGE_LOOP('',(#18339,#18340,#18341,#18342));
#3356=EDGE_LOOP('',(#18343,#18344,#18345,#18346));
#3357=EDGE_LOOP('',(#18347,#18348,#18349,#18350));
#3358=EDGE_LOOP('',(#18351,#18352,#18353,#18354));
#3359=EDGE_LOOP('',(#18355,#18356,#18357,#18358));
#3360=EDGE_LOOP('',(#18359,#18360,#18361,#18362));
#3361=EDGE_LOOP('',(#18363,#18364,#18365,#18366));
#3362=EDGE_LOOP('',(#18367,#18368,#18369,#18370));
#3363=EDGE_LOOP('',(#18371,#18372,#18373,#18374));
#3364=EDGE_LOOP('',(#18375,#18376,#18377,#18378));
#3365=EDGE_LOOP('',(#18379,#18380,#18381,#18382));
#3366=EDGE_LOOP('',(#18383,#18384,#18385,#18386));
#3367=EDGE_LOOP('',(#18387,#18388,#18389,#18390));
#3368=EDGE_LOOP('',(#18391,#18392,#18393,#18394));
#3369=EDGE_LOOP('',(#18395,#18396,#18397,#18398,#18399,#18400,#18401,#18402,
#18403,#18404,#18405,#18406,#18407,#18408,#18409,#18410,#18411,#18412,#18413,
#18414,#18415,#18416,#18417,#18418,#18419,#18420,#18421,#18422,#18423,#18424,
#18425,#18426,#18427,#18428));
#3370=EDGE_LOOP('',(#18429,#18430,#18431,#18432));
#3371=EDGE_LOOP('',(#18433,#18434,#18435,#18436));
#3372=EDGE_LOOP('',(#18437,#18438,#18439,#18440));
#3373=EDGE_LOOP('',(#18441,#18442,#18443,#18444));
#3374=EDGE_LOOP('',(#18445,#18446,#18447,#18448));
#3375=EDGE_LOOP('',(#18449,#18450,#18451,#18452));
#3376=EDGE_LOOP('',(#18453,#18454,#18455,#18456));
#3377=EDGE_LOOP('',(#18457,#18458,#18459,#18460));
#3378=EDGE_LOOP('',(#18461,#18462,#18463,#18464));
#3379=EDGE_LOOP('',(#18465,#18466,#18467,#18468));
#3380=EDGE_LOOP('',(#18469,#18470,#18471,#18472));
#3381=EDGE_LOOP('',(#18473,#18474,#18475,#18476));
#3382=EDGE_LOOP('',(#18477,#18478,#18479,#18480));
#3383=EDGE_LOOP('',(#18481,#18482,#18483,#18484));
#3384=EDGE_LOOP('',(#18485,#18486,#18487,#18488));
#3385=EDGE_LOOP('',(#18489,#18490,#18491,#18492));
#3386=EDGE_LOOP('',(#18493,#18494,#18495,#18496));
#3387=EDGE_LOOP('',(#18497,#18498,#18499,#18500));
#3388=EDGE_LOOP('',(#18501,#18502,#18503,#18504,#18505,#18506,#18507,#18508,
#18509,#18510,#18511,#18512,#18513,#18514,#18515,#18516,#18517,#18518,#18519,
#18520,#18521,#18522,#18523,#18524,#18525,#18526,#18527,#18528,#18529,#18530,
#18531,#18532,#18533,#18534));
#3957=CIRCLE('',#21842,0.450000000000145);
#3958=CIRCLE('',#21843,0.450000000000145);
#3959=CIRCLE('',#21845,2.46743797397102);
#3960=CIRCLE('',#21846,2.46743797397102);
#3961=CIRCLE('',#21848,0.725000000000007);
#3962=CIRCLE('',#21849,0.725000000000007);
#3963=CIRCLE('',#21852,0.599999999999981);
#3964=CIRCLE('',#21853,0.599999999999981);
#3965=CIRCLE('',#21855,2.3640229247478);
#3966=CIRCLE('',#21856,2.3640229247478);
#3967=CIRCLE('',#21858,1.39999999999995);
#3968=CIRCLE('',#21859,1.39999999999995);
#3969=CIRCLE('',#21862,1.05000000000001);
#3970=CIRCLE('',#21863,1.05000000000001);
#3971=CIRCLE('',#21866,1.04999999999996);
#3972=CIRCLE('',#21867,1.04999999999996);
#3973=CIRCLE('',#21870,1.09999999999999);
#3974=CIRCLE('',#21871,1.09999999999999);
#3975=CIRCLE('',#21875,0.450000000000145);
#3976=CIRCLE('',#21876,2.46743797397102);
#3977=CIRCLE('',#21877,0.725000000000007);
#3978=CIRCLE('',#21878,0.599999999999981);
#3979=CIRCLE('',#21879,2.3640229247478);
#3980=CIRCLE('',#21880,1.39999999999995);
#3981=CIRCLE('',#21881,1.05000000000001);
#3982=CIRCLE('',#21882,1.04999999999996);
#3983=CIRCLE('',#21883,1.09999999999999);
#3984=CIRCLE('',#21886,0.450000000000145);
#3985=CIRCLE('',#21888,2.46743797397102);
#3986=CIRCLE('',#21890,0.725000000000007);
#3987=CIRCLE('',#21893,0.599999999999981);
#3988=CIRCLE('',#21895,2.3640229247478);
#3989=CIRCLE('',#21897,1.39999999999995);
#3990=CIRCLE('',#21900,1.05000000000001);
#3991=CIRCLE('',#21903,1.04999999999996);
#3992=CIRCLE('',#21906,1.09999999999999);
#5808=LINE('',#48127,#7689);
#5809=LINE('',#48129,#7690);
#5810=LINE('',#48131,#7691);
#5811=LINE('',#48132,#7692);
#5812=LINE('',#48137,#7693);
#5813=LINE('',#48143,#7694);
#5814=LINE('',#48149,#7695);
#5815=LINE('',#48153,#7696);
#5816=LINE('',#48155,#7697);
#5817=LINE('',#48156,#7698);
#5818=LINE('',#48161,#7699);
#5819=LINE('',#48167,#7700);
#5820=LINE('',#48173,#7701);
#5821=LINE('',#48177,#7702);
#5822=LINE('',#48179,#7703);
#5823=LINE('',#48180,#7704);
#5824=LINE('',#48185,#7705);
#5825=LINE('',#48189,#7706);
#5826=LINE('',#48191,#7707);
#5827=LINE('',#48192,#7708);
#5828=LINE('',#48197,#7709);
#5829=LINE('',#48201,#7710);
#5830=LINE('',#48203,#7711);
#5831=LINE('',#48204,#7712);
#5832=LINE('',#48209,#7713);
#5833=LINE('',#48213,#7714);
#5834=LINE('',#48215,#7715);
#5835=LINE('',#48216,#7716);
#5836=LINE('',#48219,#7717);
#5837=LINE('',#48221,#7718);
#5838=LINE('',#48222,#7719);
#5839=LINE('',#48225,#7720);
#5840=LINE('',#48227,#7721);
#5841=LINE('',#48235,#7722);
#5842=LINE('',#48243,#7723);
#5843=LINE('',#48247,#7724);
#5844=LINE('',#48251,#7725);
#5845=LINE('',#48255,#7726);
#5846=LINE('',#48257,#7727);
#5847=LINE('',#48258,#7728);
#5848=LINE('',#48261,#7729);
#5849=LINE('',#48263,#7730);
#5850=LINE('',#48264,#7731);
#5851=LINE('',#48268,#7732);
#5852=LINE('',#48272,#7733);
#5853=LINE('',#48276,#7734);
#5854=LINE('',#48279,#7735);
#5855=LINE('',#48280,#7736);
#5856=LINE('',#48284,#7737);
#5857=LINE('',#48288,#7738);
#5858=LINE('',#48292,#7739);
#5859=LINE('',#48295,#7740);
#5860=LINE('',#48296,#7741);
#5861=LINE('',#48300,#7742);
#5862=LINE('',#48303,#7743);
#5863=LINE('',#48304,#7744);
#5864=LINE('',#48308,#7745);
#5865=LINE('',#48311,#7746);
#5866=LINE('',#48312,#7747);
#5867=LINE('',#48316,#7748);
#5868=LINE('',#48319,#7749);
#5869=LINE('',#48320,#7750);
#5870=LINE('',#48323,#7751);
#5871=LINE('',#48324,#7752);
#5872=LINE('',#48326,#7753);
#5873=LINE('',#48328,#7754);
#7689=VECTOR('',#26911,10.);
#7690=VECTOR('',#26912,10.);
#7691=VECTOR('',#26913,10.);
#7692=VECTOR('',#26914,10.);
#7693=VECTOR('',#26919,10.);
#7694=VECTOR('',#26926,10.);
#7695=VECTOR('',#26933,10.);
#7696=VECTOR('',#26938,10.);
#7697=VECTOR('',#26939,10.);
#7698=VECTOR('',#26940,10.);
#7699=VECTOR('',#26945,10.);
#7700=VECTOR('',#26952,10.);
#7701=VECTOR('',#26959,10.);
#7702=VECTOR('',#26964,10.);
#7703=VECTOR('',#26965,10.);
#7704=VECTOR('',#26966,10.);
#7705=VECTOR('',#26971,10.);
#7706=VECTOR('',#26976,10.);
#7707=VECTOR('',#26977,10.);
#7708=VECTOR('',#26978,10.);
#7709=VECTOR('',#26983,10.);
#7710=VECTOR('',#26988,10.);
#7711=VECTOR('',#26989,10.);
#7712=VECTOR('',#26990,10.);
#7713=VECTOR('',#26995,10.);
#7714=VECTOR('',#27000,10.);
#7715=VECTOR('',#27001,10.);
#7716=VECTOR('',#27002,10.);
#7717=VECTOR('',#27005,10.);
#7718=VECTOR('',#27006,10.);
#7719=VECTOR('',#27007,10.);
#7720=VECTOR('',#27010,10.);
#7721=VECTOR('',#27011,10.);
#7722=VECTOR('',#27018,10.);
#7723=VECTOR('',#27025,10.);
#7724=VECTOR('',#27028,10.);
#7725=VECTOR('',#27031,10.);
#7726=VECTOR('',#27034,10.);
#7727=VECTOR('',#27035,10.);
#7728=VECTOR('',#27036,10.);
#7729=VECTOR('',#27039,10.);
#7730=VECTOR('',#27040,10.);
#7731=VECTOR('',#27041,10.);
#7732=VECTOR('',#27046,10.);
#7733=VECTOR('',#27051,10.);
#7734=VECTOR('',#27056,10.);
#7735=VECTOR('',#27059,10.);
#7736=VECTOR('',#27060,10.);
#7737=VECTOR('',#27065,10.);
#7738=VECTOR('',#27070,10.);
#7739=VECTOR('',#27075,10.);
#7740=VECTOR('',#27078,10.);
#7741=VECTOR('',#27079,10.);
#7742=VECTOR('',#27084,10.);
#7743=VECTOR('',#27087,10.);
#7744=VECTOR('',#27088,10.);
#7745=VECTOR('',#27093,10.);
#7746=VECTOR('',#27096,10.);
#7747=VECTOR('',#27097,10.);
#7748=VECTOR('',#27102,10.);
#7749=VECTOR('',#27105,10.);
#7750=VECTOR('',#27106,10.);
#7751=VECTOR('',#27109,10.);
#7752=VECTOR('',#27110,10.);
#7753=VECTOR('',#27113,10.);
#7754=VECTOR('',#27116,10.);
#9641=VERTEX_POINT('',#48125);
#9642=VERTEX_POINT('',#48126);
#9643=VERTEX_POINT('',#48128);
#9644=VERTEX_POINT('',#48130);
#9645=VERTEX_POINT('',#48134);
#9646=VERTEX_POINT('',#48136);
#9647=VERTEX_POINT('',#48140);
#9648=VERTEX_POINT('',#48142);
#9649=VERTEX_POINT('',#48146);
#9650=VERTEX_POINT('',#48148);
#9651=VERTEX_POINT('',#48152);
#9652=VERTEX_POINT('',#48154);
#9653=VERTEX_POINT('',#48158);
#9654=VERTEX_POINT('',#48160);
#9655=VERTEX_POINT('',#48164);
#9656=VERTEX_POINT('',#48166);
#9657=VERTEX_POINT('',#48170);
#9658=VERTEX_POINT('',#48172);
#9659=VERTEX_POINT('',#48176);
#9660=VERTEX_POINT('',#48178);
#9661=VERTEX_POINT('',#48182);
#9662=VERTEX_POINT('',#48184);
#9663=VERTEX_POINT('',#48188);
#9664=VERTEX_POINT('',#48190);
#9665=VERTEX_POINT('',#48194);
#9666=VERTEX_POINT('',#48196);
#9667=VERTEX_POINT('',#48200);
#9668=VERTEX_POINT('',#48202);
#9669=VERTEX_POINT('',#48206);
#9670=VERTEX_POINT('',#48208);
#9671=VERTEX_POINT('',#48212);
#9672=VERTEX_POINT('',#48214);
#9673=VERTEX_POINT('',#48218);
#9674=VERTEX_POINT('',#48220);
#9675=VERTEX_POINT('',#48224);
#9676=VERTEX_POINT('',#48226);
#9677=VERTEX_POINT('',#48228);
#9678=VERTEX_POINT('',#48230);
#9679=VERTEX_POINT('',#48232);
#9680=VERTEX_POINT('',#48234);
#9681=VERTEX_POINT('',#48236);
#9682=VERTEX_POINT('',#48238);
#9683=VERTEX_POINT('',#48240);
#9684=VERTEX_POINT('',#48242);
#9685=VERTEX_POINT('',#48244);
#9686=VERTEX_POINT('',#48246);
#9687=VERTEX_POINT('',#48248);
#9688=VERTEX_POINT('',#48250);
#9689=VERTEX_POINT('',#48252);
#9690=VERTEX_POINT('',#48254);
#9691=VERTEX_POINT('',#48256);
#9692=VERTEX_POINT('',#48260);
#9693=VERTEX_POINT('',#48262);
#9694=VERTEX_POINT('',#48266);
#9695=VERTEX_POINT('',#48270);
#9696=VERTEX_POINT('',#48274);
#9697=VERTEX_POINT('',#48278);
#9698=VERTEX_POINT('',#48282);
#9699=VERTEX_POINT('',#48286);
#9700=VERTEX_POINT('',#48290);
#9701=VERTEX_POINT('',#48294);
#9702=VERTEX_POINT('',#48298);
#9703=VERTEX_POINT('',#48302);
#9704=VERTEX_POINT('',#48306);
#9705=VERTEX_POINT('',#48310);
#9706=VERTEX_POINT('',#48314);
#9707=VERTEX_POINT('',#48318);
#9708=VERTEX_POINT('',#48322);
#12549=EDGE_CURVE('',#9641,#9642,#5808,.T.);
#12550=EDGE_CURVE('',#9642,#9643,#5809,.T.);
#12551=EDGE_CURVE('',#9643,#9644,#5810,.T.);
#12552=EDGE_CURVE('',#9644,#9641,#5811,.T.);
#12553=EDGE_CURVE('',#9643,#9645,#3957,.T.);
#12554=EDGE_CURVE('',#9645,#9646,#5812,.T.);
#12555=EDGE_CURVE('',#9646,#9644,#3958,.T.);
#12556=EDGE_CURVE('',#9645,#9647,#3959,.T.);
#12557=EDGE_CURVE('',#9647,#9648,#5813,.T.);
#12558=EDGE_CURVE('',#9648,#9646,#3960,.T.);
#12559=EDGE_CURVE('',#9647,#9649,#3961,.T.);
#12560=EDGE_CURVE('',#9649,#9650,#5814,.T.);
#12561=EDGE_CURVE('',#9650,#9648,#3962,.T.);
#12562=EDGE_CURVE('',#9649,#9651,#5815,.T.);
#12563=EDGE_CURVE('',#9651,#9652,#5816,.T.);
#12564=EDGE_CURVE('',#9652,#9650,#5817,.T.);
#12565=EDGE_CURVE('',#9651,#9653,#3963,.T.);
#12566=EDGE_CURVE('',#9653,#9654,#5818,.T.);
#12567=EDGE_CURVE('',#9654,#9652,#3964,.T.);
#12568=EDGE_CURVE('',#9653,#9655,#3965,.T.);
#12569=EDGE_CURVE('',#9655,#9656,#5819,.T.);
#12570=EDGE_CURVE('',#9656,#9654,#3966,.T.);
#12571=EDGE_CURVE('',#9655,#9657,#3967,.T.);
#12572=EDGE_CURVE('',#9657,#9658,#5820,.T.);
#12573=EDGE_CURVE('',#9658,#9656,#3968,.T.);
#12574=EDGE_CURVE('',#9657,#9659,#5821,.T.);
#12575=EDGE_CURVE('',#9659,#9660,#5822,.T.);
#12576=EDGE_CURVE('',#9660,#9658,#5823,.T.);
#12577=EDGE_CURVE('',#9659,#9661,#3969,.T.);
#12578=EDGE_CURVE('',#9661,#9662,#5824,.T.);
#12579=EDGE_CURVE('',#9662,#9660,#3970,.T.);
#12580=EDGE_CURVE('',#9661,#9663,#5825,.T.);
#12581=EDGE_CURVE('',#9663,#9664,#5826,.T.);
#12582=EDGE_CURVE('',#9664,#9662,#5827,.T.);
#12583=EDGE_CURVE('',#9663,#9665,#3971,.T.);
#12584=EDGE_CURVE('',#9665,#9666,#5828,.T.);
#12585=EDGE_CURVE('',#9666,#9664,#3972,.T.);
#12586=EDGE_CURVE('',#9665,#9667,#5829,.T.);
#12587=EDGE_CURVE('',#9667,#9668,#5830,.T.);
#12588=EDGE_CURVE('',#9668,#9666,#5831,.T.);
#12589=EDGE_CURVE('',#9667,#9669,#3973,.T.);
#12590=EDGE_CURVE('',#9669,#9670,#5832,.T.);
#12591=EDGE_CURVE('',#9670,#9668,#3974,.T.);
#12592=EDGE_CURVE('',#9669,#9671,#5833,.T.);
#12593=EDGE_CURVE('',#9671,#9672,#5834,.T.);
#12594=EDGE_CURVE('',#9672,#9670,#5835,.T.);
#12595=EDGE_CURVE('',#9671,#9673,#5836,.T.);
#12596=EDGE_CURVE('',#9673,#9674,#5837,.T.);
#12597=EDGE_CURVE('',#9674,#9672,#5838,.T.);
#12598=EDGE_CURVE('',#9675,#9642,#5839,.T.);
#12599=EDGE_CURVE('',#9675,#9676,#5840,.T.);
#12600=EDGE_CURVE('',#9676,#9677,#3975,.T.);
#12601=EDGE_CURVE('',#9677,#9678,#3976,.T.);
#12602=EDGE_CURVE('',#9678,#9679,#3977,.T.);
#12603=EDGE_CURVE('',#9679,#9680,#5841,.T.);
#12604=EDGE_CURVE('',#9680,#9681,#3978,.T.);
#12605=EDGE_CURVE('',#9681,#9682,#3979,.T.);
#12606=EDGE_CURVE('',#9682,#9683,#3980,.T.);
#12607=EDGE_CURVE('',#9683,#9684,#5842,.T.);
#12608=EDGE_CURVE('',#9684,#9685,#3981,.T.);
#12609=EDGE_CURVE('',#9685,#9686,#5843,.T.);
#12610=EDGE_CURVE('',#9686,#9687,#3982,.T.);
#12611=EDGE_CURVE('',#9687,#9688,#5844,.T.);
#12612=EDGE_CURVE('',#9688,#9689,#3983,.T.);
#12613=EDGE_CURVE('',#9689,#9690,#5845,.T.);
#12614=EDGE_CURVE('',#9690,#9691,#5846,.T.);
#12615=EDGE_CURVE('',#9691,#9673,#5847,.T.);
#12616=EDGE_CURVE('',#9692,#9675,#5848,.T.);
#12617=EDGE_CURVE('',#9693,#9692,#5849,.T.);
#12618=EDGE_CURVE('',#9676,#9693,#5850,.T.);
#12619=EDGE_CURVE('',#9694,#9693,#3984,.T.);
#12620=EDGE_CURVE('',#9677,#9694,#5851,.T.);
#12621=EDGE_CURVE('',#9695,#9694,#3985,.T.);
#12622=EDGE_CURVE('',#9678,#9695,#5852,.T.);
#12623=EDGE_CURVE('',#9696,#9695,#3986,.T.);
#12624=EDGE_CURVE('',#9679,#9696,#5853,.T.);
#12625=EDGE_CURVE('',#9697,#9696,#5854,.T.);
#12626=EDGE_CURVE('',#9680,#9697,#5855,.T.);
#12627=EDGE_CURVE('',#9698,#9697,#3987,.T.);
#12628=EDGE_CURVE('',#9681,#9698,#5856,.T.);
#12629=EDGE_CURVE('',#9699,#9698,#3988,.T.);
#12630=EDGE_CURVE('',#9682,#9699,#5857,.T.);
#12631=EDGE_CURVE('',#9700,#9699,#3989,.T.);
#12632=EDGE_CURVE('',#9683,#9700,#5858,.T.);
#12633=EDGE_CURVE('',#9701,#9700,#5859,.T.);
#12634=EDGE_CURVE('',#9684,#9701,#5860,.T.);
#12635=EDGE_CURVE('',#9702,#9701,#3990,.T.);
#12636=EDGE_CURVE('',#9685,#9702,#5861,.T.);
#12637=EDGE_CURVE('',#9703,#9702,#5862,.T.);
#12638=EDGE_CURVE('',#9686,#9703,#5863,.T.);
#12639=EDGE_CURVE('',#9704,#9703,#3991,.T.);
#12640=EDGE_CURVE('',#9687,#9704,#5864,.T.);
#12641=EDGE_CURVE('',#9705,#9704,#5865,.T.);
#12642=EDGE_CURVE('',#9688,#9705,#5866,.T.);
#12643=EDGE_CURVE('',#9706,#9705,#3992,.T.);
#12644=EDGE_CURVE('',#9689,#9706,#5867,.T.);
#12645=EDGE_CURVE('',#9707,#9706,#5868,.T.);
#12646=EDGE_CURVE('',#9690,#9707,#5869,.T.);
#12647=EDGE_CURVE('',#9708,#9707,#5870,.T.);
#12648=EDGE_CURVE('',#9691,#9708,#5871,.T.);
#12649=EDGE_CURVE('',#9708,#9674,#5872,.T.);
#12650=EDGE_CURVE('',#9692,#9641,#5873,.T.);
#18331=ORIENTED_EDGE('',*,*,#12549,.T.);
#18332=ORIENTED_EDGE('',*,*,#12550,.T.);
#18333=ORIENTED_EDGE('',*,*,#12551,.T.);
#18334=ORIENTED_EDGE('',*,*,#12552,.T.);
#18335=ORIENTED_EDGE('',*,*,#12551,.F.);
#18336=ORIENTED_EDGE('',*,*,#12553,.T.);
#18337=ORIENTED_EDGE('',*,*,#12554,.T.);
#18338=ORIENTED_EDGE('',*,*,#12555,.T.);
#18339=ORIENTED_EDGE('',*,*,#12554,.F.);
#18340=ORIENTED_EDGE('',*,*,#12556,.T.);
#18341=ORIENTED_EDGE('',*,*,#12557,.T.);
#18342=ORIENTED_EDGE('',*,*,#12558,.T.);
#18343=ORIENTED_EDGE('',*,*,#12557,.F.);
#18344=ORIENTED_EDGE('',*,*,#12559,.T.);
#18345=ORIENTED_EDGE('',*,*,#12560,.T.);
#18346=ORIENTED_EDGE('',*,*,#12561,.T.);
#18347=ORIENTED_EDGE('',*,*,#12560,.F.);
#18348=ORIENTED_EDGE('',*,*,#12562,.T.);
#18349=ORIENTED_EDGE('',*,*,#12563,.T.);
#18350=ORIENTED_EDGE('',*,*,#12564,.T.);
#18351=ORIENTED_EDGE('',*,*,#12563,.F.);
#18352=ORIENTED_EDGE('',*,*,#12565,.T.);
#18353=ORIENTED_EDGE('',*,*,#12566,.T.);
#18354=ORIENTED_EDGE('',*,*,#12567,.T.);
#18355=ORIENTED_EDGE('',*,*,#12566,.F.);
#18356=ORIENTED_EDGE('',*,*,#12568,.T.);
#18357=ORIENTED_EDGE('',*,*,#12569,.T.);
#18358=ORIENTED_EDGE('',*,*,#12570,.T.);
#18359=ORIENTED_EDGE('',*,*,#12569,.F.);
#18360=ORIENTED_EDGE('',*,*,#12571,.T.);
#18361=ORIENTED_EDGE('',*,*,#12572,.T.);
#18362=ORIENTED_EDGE('',*,*,#12573,.T.);
#18363=ORIENTED_EDGE('',*,*,#12572,.F.);
#18364=ORIENTED_EDGE('',*,*,#12574,.T.);
#18365=ORIENTED_EDGE('',*,*,#12575,.T.);
#18366=ORIENTED_EDGE('',*,*,#12576,.T.);
#18367=ORIENTED_EDGE('',*,*,#12575,.F.);
#18368=ORIENTED_EDGE('',*,*,#12577,.T.);
#18369=ORIENTED_EDGE('',*,*,#12578,.T.);
#18370=ORIENTED_EDGE('',*,*,#12579,.T.);
#18371=ORIENTED_EDGE('',*,*,#12578,.F.);
#18372=ORIENTED_EDGE('',*,*,#12580,.T.);
#18373=ORIENTED_EDGE('',*,*,#12581,.T.);
#18374=ORIENTED_EDGE('',*,*,#12582,.T.);
#18375=ORIENTED_EDGE('',*,*,#12581,.F.);
#18376=ORIENTED_EDGE('',*,*,#12583,.T.);
#18377=ORIENTED_EDGE('',*,*,#12584,.T.);
#18378=ORIENTED_EDGE('',*,*,#12585,.T.);
#18379=ORIENTED_EDGE('',*,*,#12584,.F.);
#18380=ORIENTED_EDGE('',*,*,#12586,.T.);
#18381=ORIENTED_EDGE('',*,*,#12587,.T.);
#18382=ORIENTED_EDGE('',*,*,#12588,.T.);
#18383=ORIENTED_EDGE('',*,*,#12587,.F.);
#18384=ORIENTED_EDGE('',*,*,#12589,.T.);
#18385=ORIENTED_EDGE('',*,*,#12590,.T.);
#18386=ORIENTED_EDGE('',*,*,#12591,.T.);
#18387=ORIENTED_EDGE('',*,*,#12590,.F.);
#18388=ORIENTED_EDGE('',*,*,#12592,.T.);
#18389=ORIENTED_EDGE('',*,*,#12593,.T.);
#18390=ORIENTED_EDGE('',*,*,#12594,.T.);
#18391=ORIENTED_EDGE('',*,*,#12593,.F.);
#18392=ORIENTED_EDGE('',*,*,#12595,.T.);
#18393=ORIENTED_EDGE('',*,*,#12596,.T.);
#18394=ORIENTED_EDGE('',*,*,#12597,.T.);
#18395=ORIENTED_EDGE('',*,*,#12598,.F.);
#18396=ORIENTED_EDGE('',*,*,#12599,.T.);
#18397=ORIENTED_EDGE('',*,*,#12600,.T.);
#18398=ORIENTED_EDGE('',*,*,#12601,.T.);
#18399=ORIENTED_EDGE('',*,*,#12602,.T.);
#18400=ORIENTED_EDGE('',*,*,#12603,.T.);
#18401=ORIENTED_EDGE('',*,*,#12604,.T.);
#18402=ORIENTED_EDGE('',*,*,#12605,.T.);
#18403=ORIENTED_EDGE('',*,*,#12606,.T.);
#18404=ORIENTED_EDGE('',*,*,#12607,.T.);
#18405=ORIENTED_EDGE('',*,*,#12608,.T.);
#18406=ORIENTED_EDGE('',*,*,#12609,.T.);
#18407=ORIENTED_EDGE('',*,*,#12610,.T.);
#18408=ORIENTED_EDGE('',*,*,#12611,.T.);
#18409=ORIENTED_EDGE('',*,*,#12612,.T.);
#18410=ORIENTED_EDGE('',*,*,#12613,.T.);
#18411=ORIENTED_EDGE('',*,*,#12614,.T.);
#18412=ORIENTED_EDGE('',*,*,#12615,.T.);
#18413=ORIENTED_EDGE('',*,*,#12595,.F.);
#18414=ORIENTED_EDGE('',*,*,#12592,.F.);
#18415=ORIENTED_EDGE('',*,*,#12589,.F.);
#18416=ORIENTED_EDGE('',*,*,#12586,.F.);
#18417=ORIENTED_EDGE('',*,*,#12583,.F.);
#18418=ORIENTED_EDGE('',*,*,#12580,.F.);
#18419=ORIENTED_EDGE('',*,*,#12577,.F.);
#18420=ORIENTED_EDGE('',*,*,#12574,.F.);
#18421=ORIENTED_EDGE('',*,*,#12571,.F.);
#18422=ORIENTED_EDGE('',*,*,#12568,.F.);
#18423=ORIENTED_EDGE('',*,*,#12565,.F.);
#18424=ORIENTED_EDGE('',*,*,#12562,.F.);
#18425=ORIENTED_EDGE('',*,*,#12559,.F.);
#18426=ORIENTED_EDGE('',*,*,#12556,.F.);
#18427=ORIENTED_EDGE('',*,*,#12553,.F.);
#18428=ORIENTED_EDGE('',*,*,#12550,.F.);
#18429=ORIENTED_EDGE('',*,*,#12616,.F.);
#18430=ORIENTED_EDGE('',*,*,#12617,.F.);
#18431=ORIENTED_EDGE('',*,*,#12618,.F.);
#18432=ORIENTED_EDGE('',*,*,#12599,.F.);
#18433=ORIENTED_EDGE('',*,*,#12618,.T.);
#18434=ORIENTED_EDGE('',*,*,#12619,.F.);
#18435=ORIENTED_EDGE('',*,*,#12620,.F.);
#18436=ORIENTED_EDGE('',*,*,#12600,.F.);
#18437=ORIENTED_EDGE('',*,*,#12620,.T.);
#18438=ORIENTED_EDGE('',*,*,#12621,.F.);
#18439=ORIENTED_EDGE('',*,*,#12622,.F.);
#18440=ORIENTED_EDGE('',*,*,#12601,.F.);
#18441=ORIENTED_EDGE('',*,*,#12622,.T.);
#18442=ORIENTED_EDGE('',*,*,#12623,.F.);
#18443=ORIENTED_EDGE('',*,*,#12624,.F.);
#18444=ORIENTED_EDGE('',*,*,#12602,.F.);
#18445=ORIENTED_EDGE('',*,*,#12624,.T.);
#18446=ORIENTED_EDGE('',*,*,#12625,.F.);
#18447=ORIENTED_EDGE('',*,*,#12626,.F.);
#18448=ORIENTED_EDGE('',*,*,#12603,.F.);
#18449=ORIENTED_EDGE('',*,*,#12626,.T.);
#18450=ORIENTED_EDGE('',*,*,#12627,.F.);
#18451=ORIENTED_EDGE('',*,*,#12628,.F.);
#18452=ORIENTED_EDGE('',*,*,#12604,.F.);
#18453=ORIENTED_EDGE('',*,*,#12628,.T.);
#18454=ORIENTED_EDGE('',*,*,#12629,.F.);
#18455=ORIENTED_EDGE('',*,*,#12630,.F.);
#18456=ORIENTED_EDGE('',*,*,#12605,.F.);
#18457=ORIENTED_EDGE('',*,*,#12630,.T.);
#18458=ORIENTED_EDGE('',*,*,#12631,.F.);
#18459=ORIENTED_EDGE('',*,*,#12632,.F.);
#18460=ORIENTED_EDGE('',*,*,#12606,.F.);
#18461=ORIENTED_EDGE('',*,*,#12632,.T.);
#18462=ORIENTED_EDGE('',*,*,#12633,.F.);
#18463=ORIENTED_EDGE('',*,*,#12634,.F.);
#18464=ORIENTED_EDGE('',*,*,#12607,.F.);
#18465=ORIENTED_EDGE('',*,*,#12634,.T.);
#18466=ORIENTED_EDGE('',*,*,#12635,.F.);
#18467=ORIENTED_EDGE('',*,*,#12636,.F.);
#18468=ORIENTED_EDGE('',*,*,#12608,.F.);
#18469=ORIENTED_EDGE('',*,*,#12636,.T.);
#18470=ORIENTED_EDGE('',*,*,#12637,.F.);
#18471=ORIENTED_EDGE('',*,*,#12638,.F.);
#18472=ORIENTED_EDGE('',*,*,#12609,.F.);
#18473=ORIENTED_EDGE('',*,*,#12638,.T.);
#18474=ORIENTED_EDGE('',*,*,#12639,.F.);
#18475=ORIENTED_EDGE('',*,*,#12640,.F.);
#18476=ORIENTED_EDGE('',*,*,#12610,.F.);
#18477=ORIENTED_EDGE('',*,*,#12640,.T.);
#18478=ORIENTED_EDGE('',*,*,#12641,.F.);
#18479=ORIENTED_EDGE('',*,*,#12642,.F.);
#18480=ORIENTED_EDGE('',*,*,#12611,.F.);
#18481=ORIENTED_EDGE('',*,*,#12642,.T.);
#18482=ORIENTED_EDGE('',*,*,#12643,.F.);
#18483=ORIENTED_EDGE('',*,*,#12644,.F.);
#18484=ORIENTED_EDGE('',*,*,#12612,.F.);
#18485=ORIENTED_EDGE('',*,*,#12644,.T.);
#18486=ORIENTED_EDGE('',*,*,#12645,.F.);
#18487=ORIENTED_EDGE('',*,*,#12646,.F.);
#18488=ORIENTED_EDGE('',*,*,#12613,.F.);
#18489=ORIENTED_EDGE('',*,*,#12646,.T.);
#18490=ORIENTED_EDGE('',*,*,#12647,.F.);
#18491=ORIENTED_EDGE('',*,*,#12648,.F.);
#18492=ORIENTED_EDGE('',*,*,#12614,.F.);
#18493=ORIENTED_EDGE('',*,*,#12648,.T.);
#18494=ORIENTED_EDGE('',*,*,#12649,.T.);
#18495=ORIENTED_EDGE('',*,*,#12596,.F.);
#18496=ORIENTED_EDGE('',*,*,#12615,.F.);
#18497=ORIENTED_EDGE('',*,*,#12650,.F.);
#18498=ORIENTED_EDGE('',*,*,#12616,.T.);
#18499=ORIENTED_EDGE('',*,*,#12598,.T.);
#18500=ORIENTED_EDGE('',*,*,#12549,.F.);
#18501=ORIENTED_EDGE('',*,*,#12650,.T.);
#18502=ORIENTED_EDGE('',*,*,#12552,.F.);
#18503=ORIENTED_EDGE('',*,*,#12555,.F.);
#18504=ORIENTED_EDGE('',*,*,#12558,.F.);
#18505=ORIENTED_EDGE('',*,*,#12561,.F.);
#18506=ORIENTED_EDGE('',*,*,#12564,.F.);
#18507=ORIENTED_EDGE('',*,*,#12567,.F.);
#18508=ORIENTED_EDGE('',*,*,#12570,.F.);
#18509=ORIENTED_EDGE('',*,*,#12573,.F.);
#18510=ORIENTED_EDGE('',*,*,#12576,.F.);
#18511=ORIENTED_EDGE('',*,*,#12579,.F.);
#18512=ORIENTED_EDGE('',*,*,#12582,.F.);
#18513=ORIENTED_EDGE('',*,*,#12585,.F.);
#18514=ORIENTED_EDGE('',*,*,#12588,.F.);
#18515=ORIENTED_EDGE('',*,*,#12591,.F.);
#18516=ORIENTED_EDGE('',*,*,#12594,.F.);
#18517=ORIENTED_EDGE('',*,*,#12597,.F.);
#18518=ORIENTED_EDGE('',*,*,#12649,.F.);
#18519=ORIENTED_EDGE('',*,*,#12647,.T.);
#18520=ORIENTED_EDGE('',*,*,#12645,.T.);
#18521=ORIENTED_EDGE('',*,*,#12643,.T.);
#18522=ORIENTED_EDGE('',*,*,#12641,.T.);
#18523=ORIENTED_EDGE('',*,*,#12639,.T.);
#18524=ORIENTED_EDGE('',*,*,#12637,.T.);
#18525=ORIENTED_EDGE('',*,*,#12635,.T.);
#18526=ORIENTED_EDGE('',*,*,#12633,.T.);
#18527=ORIENTED_EDGE('',*,*,#12631,.T.);
#18528=ORIENTED_EDGE('',*,*,#12629,.T.);
#18529=ORIENTED_EDGE('',*,*,#12627,.T.);
#18530=ORIENTED_EDGE('',*,*,#12625,.T.);
#18531=ORIENTED_EDGE('',*,*,#12623,.T.);
#18532=ORIENTED_EDGE('',*,*,#12621,.T.);
#18533=ORIENTED_EDGE('',*,*,#12619,.T.);
#18534=ORIENTED_EDGE('',*,*,#12617,.T.);
#19046=PLANE('',#21840);
#19047=PLANE('',#21850);
#19048=PLANE('',#21860);
#19049=PLANE('',#21864);
#19050=PLANE('',#21868);
#19051=PLANE('',#21872);
#19052=PLANE('',#21873);
#19053=PLANE('',#21874);
#19054=PLANE('',#21884);
#19055=PLANE('',#21891);
#19056=PLANE('',#21898);
#19057=PLANE('',#21901);
#19058=PLANE('',#21904);
#19059=PLANE('',#21907);
#19060=PLANE('',#21908);
#19061=PLANE('',#21909);
#19062=PLANE('',#21910);
#19063=PLANE('',#21911);
#20072=ADVANCED_FACE('',(#2215),#19046,.F.);
#20073=ADVANCED_FACE('',(#2216),#1189,.T.);
#20074=ADVANCED_FACE('',(#2217),#1190,.F.);
#20075=ADVANCED_FACE('',(#2218),#1191,.T.);
#20076=ADVANCED_FACE('',(#2219),#19047,.F.);
#20077=ADVANCED_FACE('',(#2220),#1192,.T.);
#20078=ADVANCED_FACE('',(#2221),#1193,.F.);
#20079=ADVANCED_FACE('',(#2222),#1194,.T.);
#20080=ADVANCED_FACE('',(#2223),#19048,.F.);
#20081=ADVANCED_FACE('',(#2224),#1195,.F.);
#20082=ADVANCED_FACE('',(#2225),#19049,.F.);
#20083=ADVANCED_FACE('',(#2226),#1196,.F.);
#20084=ADVANCED_FACE('',(#2227),#19050,.F.);
#20085=ADVANCED_FACE('',(#2228),#1197,.T.);
#20086=ADVANCED_FACE('',(#2229),#19051,.F.);
#20087=ADVANCED_FACE('',(#2230),#19052,.F.);
#20088=ADVANCED_FACE('',(#2231),#19053,.F.);
#20089=ADVANCED_FACE('',(#2232),#19054,.T.);
#20090=ADVANCED_FACE('',(#2233),#1198,.T.);
#20091=ADVANCED_FACE('',(#2234),#1199,.F.);
#20092=ADVANCED_FACE('',(#2235),#1200,.T.);
#20093=ADVANCED_FACE('',(#2236),#19055,.T.);
#20094=ADVANCED_FACE('',(#2237),#1201,.T.);
#20095=ADVANCED_FACE('',(#2238),#1202,.F.);
#20096=ADVANCED_FACE('',(#2239),#1203,.T.);
#20097=ADVANCED_FACE('',(#2240),#19056,.T.);
#20098=ADVANCED_FACE('',(#2241),#1204,.F.);
#20099=ADVANCED_FACE('',(#2242),#19057,.T.);
#20100=ADVANCED_FACE('',(#2243),#1205,.F.);
#20101=ADVANCED_FACE('',(#2244),#19058,.T.);
#20102=ADVANCED_FACE('',(#2245),#1206,.T.);
#20103=ADVANCED_FACE('',(#2246),#19059,.T.);
#20104=ADVANCED_FACE('',(#2247),#19060,.T.);
#20105=ADVANCED_FACE('',(#2248),#19061,.T.);
#20106=ADVANCED_FACE('',(#2249),#19062,.T.);
#20107=ADVANCED_FACE('',(#2250),#19063,.T.);
#20133=CLOSED_SHELL('',(#20072,#20073,#20074,#20075,#20076,#20077,#20078,
#20079,#20080,#20081,#20082,#20083,#20084,#20085,#20086,#20087,#20088,#20089,
#20090,#20091,#20092,#20093,#20094,#20095,#20096,#20097,#20098,#20099,#20100,
#20101,#20102,#20103,#20104,#20105,#20106,#20107));
#21839=AXIS2_PLACEMENT_3D('',#48123,#26907,#26908);
#21840=AXIS2_PLACEMENT_3D('',#48124,#26909,#26910);
#21841=AXIS2_PLACEMENT_3D('',#48133,#26915,#26916);
#21842=AXIS2_PLACEMENT_3D('',#48135,#26917,#26918);
#21843=AXIS2_PLACEMENT_3D('',#48138,#26920,#26921);
#21844=AXIS2_PLACEMENT_3D('',#48139,#26922,#26923);
#21845=AXIS2_PLACEMENT_3D('',#48141,#26924,#26925);
#21846=AXIS2_PLACEMENT_3D('',#48144,#26927,#26928);
#21847=AXIS2_PLACEMENT_3D('',#48145,#26929,#26930);
#21848=AXIS2_PLACEMENT_3D('',#48147,#26931,#26932);
#21849=AXIS2_PLACEMENT_3D('',#48150,#26934,#26935);
#21850=AXIS2_PLACEMENT_3D('',#48151,#26936,#26937);
#21851=AXIS2_PLACEMENT_3D('',#48157,#26941,#26942);
#21852=AXIS2_PLACEMENT_3D('',#48159,#26943,#26944);
#21853=AXIS2_PLACEMENT_3D('',#48162,#26946,#26947);
#21854=AXIS2_PLACEMENT_3D('',#48163,#26948,#26949);
#21855=AXIS2_PLACEMENT_3D('',#48165,#26950,#26951);
#21856=AXIS2_PLACEMENT_3D('',#48168,#26953,#26954);
#21857=AXIS2_PLACEMENT_3D('',#48169,#26955,#26956);
#21858=AXIS2_PLACEMENT_3D('',#48171,#26957,#26958);
#21859=AXIS2_PLACEMENT_3D('',#48174,#26960,#26961);
#21860=AXIS2_PLACEMENT_3D('',#48175,#26962,#26963);
#21861=AXIS2_PLACEMENT_3D('',#48181,#26967,#26968);
#21862=AXIS2_PLACEMENT_3D('',#48183,#26969,#26970);
#21863=AXIS2_PLACEMENT_3D('',#48186,#26972,#26973);
#21864=AXIS2_PLACEMENT_3D('',#48187,#26974,#26975);
#21865=AXIS2_PLACEMENT_3D('',#48193,#26979,#26980);
#21866=AXIS2_PLACEMENT_3D('',#48195,#26981,#26982);
#21867=AXIS2_PLACEMENT_3D('',#48198,#26984,#26985);
#21868=AXIS2_PLACEMENT_3D('',#48199,#26986,#26987);
#21869=AXIS2_PLACEMENT_3D('',#48205,#26991,#26992);
#21870=AXIS2_PLACEMENT_3D('',#48207,#26993,#26994);
#21871=AXIS2_PLACEMENT_3D('',#48210,#26996,#26997);
#21872=AXIS2_PLACEMENT_3D('',#48211,#26998,#26999);
#21873=AXIS2_PLACEMENT_3D('',#48217,#27003,#27004);
#21874=AXIS2_PLACEMENT_3D('',#48223,#27008,#27009);
#21875=AXIS2_PLACEMENT_3D('',#48229,#27012,#27013);
#21876=AXIS2_PLACEMENT_3D('',#48231,#27014,#27015);
#21877=AXIS2_PLACEMENT_3D('',#48233,#27016,#27017);
#21878=AXIS2_PLACEMENT_3D('',#48237,#27019,#27020);
#21879=AXIS2_PLACEMENT_3D('',#48239,#27021,#27022);
#21880=AXIS2_PLACEMENT_3D('',#48241,#27023,#27024);
#21881=AXIS2_PLACEMENT_3D('',#48245,#27026,#27027);
#21882=AXIS2_PLACEMENT_3D('',#48249,#27029,#27030);
#21883=AXIS2_PLACEMENT_3D('',#48253,#27032,#27033);
#21884=AXIS2_PLACEMENT_3D('',#48259,#27037,#27038);
#21885=AXIS2_PLACEMENT_3D('',#48265,#27042,#27043);
#21886=AXIS2_PLACEMENT_3D('',#48267,#27044,#27045);
#21887=AXIS2_PLACEMENT_3D('',#48269,#27047,#27048);
#21888=AXIS2_PLACEMENT_3D('',#48271,#27049,#27050);
#21889=AXIS2_PLACEMENT_3D('',#48273,#27052,#27053);
#21890=AXIS2_PLACEMENT_3D('',#48275,#27054,#27055);
#21891=AXIS2_PLACEMENT_3D('',#48277,#27057,#27058);
#21892=AXIS2_PLACEMENT_3D('',#48281,#27061,#27062);
#21893=AXIS2_PLACEMENT_3D('',#48283,#27063,#27064);
#21894=AXIS2_PLACEMENT_3D('',#48285,#27066,#27067);
#21895=AXIS2_PLACEMENT_3D('',#48287,#27068,#27069);
#21896=AXIS2_PLACEMENT_3D('',#48289,#27071,#27072);
#21897=AXIS2_PLACEMENT_3D('',#48291,#27073,#27074);
#21898=AXIS2_PLACEMENT_3D('',#48293,#27076,#27077);
#21899=AXIS2_PLACEMENT_3D('',#48297,#27080,#27081);
#21900=AXIS2_PLACEMENT_3D('',#48299,#27082,#27083);
#21901=AXIS2_PLACEMENT_3D('',#48301,#27085,#27086);
#21902=AXIS2_PLACEMENT_3D('',#48305,#27089,#27090);
#21903=AXIS2_PLACEMENT_3D('',#48307,#27091,#27092);
#21904=AXIS2_PLACEMENT_3D('',#48309,#27094,#27095);
#21905=AXIS2_PLACEMENT_3D('',#48313,#27098,#27099);
#21906=AXIS2_PLACEMENT_3D('',#48315,#27100,#27101);
#21907=AXIS2_PLACEMENT_3D('',#48317,#27103,#27104);
#21908=AXIS2_PLACEMENT_3D('',#48321,#27107,#27108);
#21909=AXIS2_PLACEMENT_3D('',#48325,#27111,#27112);
#21910=AXIS2_PLACEMENT_3D('',#48327,#27114,#27115);
#21911=AXIS2_PLACEMENT_3D('',#48329,#27117,#27118);
#26907=DIRECTION('axis',(0.,0.,1.));
#26908=DIRECTION('refdir',(1.,0.,0.));
#26909=DIRECTION('center_axis',(0.710729249896214,0.,-0.703465658964221));
#26910=DIRECTION('ref_axis',(0.703465658964221,0.,0.710729249896214));
#26911=DIRECTION('',(0.,1.,0.));
#26912=DIRECTION('',(-0.703465658964221,0.,-0.710729249896214));
#26913=DIRECTION('',(0.,-1.,0.));
#26914=DIRECTION('',(0.703465658964221,0.,0.710729249896214));
#26915=DIRECTION('center_axis',(0.,1.,0.));
#26916=DIRECTION('ref_axis',(-0.963381374692954,0.,0.268134904282738));
#26917=DIRECTION('center_axis',(0.,-1.,0.));
#26918=DIRECTION('ref_axis',(-0.963381374692954,0.,0.268134904282738));
#26919=DIRECTION('',(0.,-1.,0.));
#26920=DIRECTION('center_axis',(0.,1.,0.));
#26921=DIRECTION('ref_axis',(-0.963381374692954,0.,0.268134904282738));
#26922=DIRECTION('center_axis',(0.,1.,0.));
#26923=DIRECTION('ref_axis',(0.963381374692978,0.,-0.268134904282653));
#26924=DIRECTION('center_axis',(0.,1.,0.));
#26925=DIRECTION('ref_axis',(0.963381374692978,0.,-0.268134904282653));
#26926=DIRECTION('',(0.,-1.,0.));
#26927=DIRECTION('center_axis',(0.,-1.,0.));
#26928=DIRECTION('ref_axis',(0.963381374692978,0.,-0.268134904282653));
#26929=DIRECTION('center_axis',(0.,1.,0.));
#26930=DIRECTION('ref_axis',(-1.,0.,-2.53764096072769E-16));
#26931=DIRECTION('center_axis',(0.,-1.,0.));
#26932=DIRECTION('ref_axis',(-1.,0.,-2.53764096072769E-16));
#26933=DIRECTION('',(0.,-1.,0.));
#26934=DIRECTION('center_axis',(0.,1.,0.));
#26935=DIRECTION('ref_axis',(-1.,0.,-2.53764096072769E-16));
#26936=DIRECTION('center_axis',(1.,0.,2.53764096072769E-16));
#26937=DIRECTION('ref_axis',(-2.53764096072769E-16,0.,1.));
#26938=DIRECTION('',(2.53764096072769E-16,0.,-1.));
#26939=DIRECTION('',(0.,-1.,0.));
#26940=DIRECTION('',(-2.53764096072769E-16,0.,1.));
#26941=DIRECTION('center_axis',(0.,1.,0.));
#26942=DIRECTION('ref_axis',(-0.245760053518537,0.,-0.969330694909929));
#26943=DIRECTION('center_axis',(0.,-1.,0.));
#26944=DIRECTION('ref_axis',(-0.245760053518537,0.,-0.969330694909929));
#26945=DIRECTION('',(0.,-1.,0.));
#26946=DIRECTION('center_axis',(0.,1.,0.));
#26947=DIRECTION('ref_axis',(-0.245760053518537,0.,-0.969330694909929));
#26948=DIRECTION('center_axis',(0.,1.,0.));
#26949=DIRECTION('ref_axis',(0.245760053518569,0.,0.969330694909921));
#26950=DIRECTION('center_axis',(0.,1.,0.));
#26951=DIRECTION('ref_axis',(0.245760053518569,0.,0.969330694909921));
#26952=DIRECTION('',(0.,-1.,0.));
#26953=DIRECTION('center_axis',(0.,-1.,0.));
#26954=DIRECTION('ref_axis',(0.245760053518569,0.,0.969330694909921));
#26955=DIRECTION('center_axis',(0.,1.,0.));
#26956=DIRECTION('ref_axis',(-0.711979844231348,0.,-0.702199901316075));
#26957=DIRECTION('center_axis',(0.,-1.,0.));
#26958=DIRECTION('ref_axis',(-0.711979844231348,0.,-0.702199901316075));
#26959=DIRECTION('',(0.,-1.,0.));
#26960=DIRECTION('center_axis',(0.,1.,0.));
#26961=DIRECTION('ref_axis',(-0.711979844231348,0.,-0.702199901316075));
#26962=DIRECTION('center_axis',(0.71197984423134,0.,0.702199901316083));
#26963=DIRECTION('ref_axis',(-0.702199901316083,0.,0.71197984423134));
#26964=DIRECTION('',(0.702199901316083,0.,-0.71197984423134));
#26965=DIRECTION('',(0.,-1.,0.));
#26966=DIRECTION('',(-0.702199901316083,0.,0.71197984423134));
#26967=DIRECTION('center_axis',(0.,1.,0.));
#26968=DIRECTION('ref_axis',(0.711979844231334,0.,0.702199901316089));
#26969=DIRECTION('center_axis',(0.,1.,0.));
#26970=DIRECTION('ref_axis',(0.711979844231334,0.,0.702199901316089));
#26971=DIRECTION('',(0.,-1.,0.));
#26972=DIRECTION('center_axis',(0.,-1.,0.));
#26973=DIRECTION('ref_axis',(0.711979844231334,0.,0.702199901316089));
#26974=DIRECTION('center_axis',(1.,0.,2.53764096072769E-16));
#26975=DIRECTION('ref_axis',(-2.53764096072769E-16,0.,1.));
#26976=DIRECTION('',(2.53764096072769E-16,0.,-1.));
#26977=DIRECTION('',(0.,-1.,0.));
#26978=DIRECTION('',(-2.53764096072769E-16,0.,1.));
#26979=DIRECTION('center_axis',(0.,1.,0.));
#26980=DIRECTION('ref_axis',(1.,0.,1.71714482808377E-14));
#26981=DIRECTION('center_axis',(0.,1.,0.));
#26982=DIRECTION('ref_axis',(1.,0.,1.71714482808377E-14));
#26983=DIRECTION('',(0.,-1.,0.));
#26984=DIRECTION('center_axis',(0.,-1.,0.));
#26985=DIRECTION('ref_axis',(1.,0.,1.71714482808377E-14));
#26986=DIRECTION('center_axis',(0.709478283082607,0.,-0.704727298913669));
#26987=DIRECTION('ref_axis',(0.704727298913669,0.,0.709478283082607));
#26988=DIRECTION('',(-0.704727298913669,0.,-0.709478283082607));
#26989=DIRECTION('',(0.,-1.,0.));
#26990=DIRECTION('',(0.704727298913669,0.,0.709478283082607));
#26991=DIRECTION('center_axis',(0.,1.,0.));
#26992=DIRECTION('ref_axis',(-1.,0.,-4.29093873107336E-15));
#26993=DIRECTION('center_axis',(0.,-1.,0.));
#26994=DIRECTION('ref_axis',(-1.,0.,-4.29093873107336E-15));
#26995=DIRECTION('',(0.,-1.,0.));
#26996=DIRECTION('center_axis',(0.,1.,0.));
#26997=DIRECTION('ref_axis',(-1.,0.,-4.29093873107336E-15));
#26998=DIRECTION('center_axis',(1.,0.,2.53764096072769E-16));
#26999=DIRECTION('ref_axis',(-2.53764096072769E-16,0.,1.));
#27000=DIRECTION('',(2.53764096072769E-16,0.,-1.));
#27001=DIRECTION('',(0.,-1.,0.));
#27002=DIRECTION('',(-2.53764096072769E-16,0.,1.));
#27003=DIRECTION('center_axis',(0.707376432457449,0.,0.706837027046385));
#27004=DIRECTION('ref_axis',(-0.706837027046385,0.,0.707376432457449));
#27005=DIRECTION('',(0.706837027046385,0.,-0.707376432457449));
#27006=DIRECTION('',(0.,-1.,0.));
#27007=DIRECTION('',(-0.706837027046385,0.,0.707376432457449));
#27008=DIRECTION('center_axis',(0.,-1.,0.));
#27009=DIRECTION('ref_axis',(-1.,0.,0.));
#27010=DIRECTION('',(-1.,0.,-2.53764096072769E-16));
#27011=DIRECTION('',(0.703465658964221,0.,-0.710729249896213));
#27012=DIRECTION('center_axis',(0.,1.,0.));
#27013=DIRECTION('ref_axis',(0.963381374692954,0.,0.268134904282739));
#27014=DIRECTION('center_axis',(0.,-1.,0.));
#27015=DIRECTION('ref_axis',(-0.963381374692978,0.,-0.268134904282653));
#27016=DIRECTION('center_axis',(0.,1.,0.));
#27017=DIRECTION('ref_axis',(1.,0.,0.));
#27018=DIRECTION('',(0.,0.,-1.));
#27019=DIRECTION('center_axis',(0.,1.,0.));
#27020=DIRECTION('ref_axis',(0.245760053518537,0.,-0.969330694909929));
#27021=DIRECTION('center_axis',(0.,-1.,0.));
#27022=DIRECTION('ref_axis',(-0.245760053518569,0.,0.969330694909921));
#27023=DIRECTION('center_axis',(0.,1.,0.));
#27024=DIRECTION('ref_axis',(0.711979844231348,0.,-0.702199901316075));
#27025=DIRECTION('',(-0.702199901316083,0.,-0.71197984423134));
#27026=DIRECTION('center_axis',(0.,-1.,0.));
#27027=DIRECTION('ref_axis',(-0.711979844231334,0.,0.702199901316089));
#27028=DIRECTION('',(0.,0.,-1.));
#27029=DIRECTION('center_axis',(0.,-1.,0.));
#27030=DIRECTION('ref_axis',(-1.,0.,1.69176841847649E-14));
#27031=DIRECTION('',(0.704727298913669,0.,-0.709478283082607));
#27032=DIRECTION('center_axis',(0.,1.,0.));
#27033=DIRECTION('ref_axis',(1.,0.,-4.03717463500059E-15));
#27034=DIRECTION('',(0.,0.,-1.));
#27035=DIRECTION('',(-0.706837027046385,0.,-0.707376432457449));
#27036=DIRECTION('',(-1.,0.,0.));
#27037=DIRECTION('center_axis',(0.710729249896213,0.,0.703465658964221));
#27038=DIRECTION('ref_axis',(-0.703465658964221,0.,0.710729249896213));
#27039=DIRECTION('',(0.,1.,0.));
#27040=DIRECTION('',(-0.703465658964221,0.,0.710729249896213));
#27041=DIRECTION('',(0.,-1.,0.));
#27042=DIRECTION('center_axis',(0.,-1.,0.));
#27043=DIRECTION('ref_axis',(0.963381374692954,0.,0.268134904282739));
#27044=DIRECTION('center_axis',(0.,-1.,0.));
#27045=DIRECTION('ref_axis',(0.963381374692954,0.,0.268134904282739));
#27046=DIRECTION('',(0.,-1.,0.));
#27047=DIRECTION('center_axis',(0.,-1.,0.));
#27048=DIRECTION('ref_axis',(-0.963381374692978,0.,-0.268134904282653));
#27049=DIRECTION('center_axis',(0.,1.,0.));
#27050=DIRECTION('ref_axis',(-0.963381374692978,0.,-0.268134904282653));
#27051=DIRECTION('',(0.,-1.,0.));
#27052=DIRECTION('center_axis',(0.,-1.,0.));
#27053=DIRECTION('ref_axis',(1.,0.,0.));
#27054=DIRECTION('center_axis',(0.,-1.,0.));
#27055=DIRECTION('ref_axis',(1.,0.,0.));
#27056=DIRECTION('',(0.,-1.,0.));
#27057=DIRECTION('center_axis',(1.,0.,0.));
#27058=DIRECTION('ref_axis',(0.,0.,1.));
#27059=DIRECTION('',(0.,0.,1.));
#27060=DIRECTION('',(0.,-1.,0.));
#27061=DIRECTION('center_axis',(0.,-1.,0.));
#27062=DIRECTION('ref_axis',(0.245760053518537,0.,-0.969330694909929));
#27063=DIRECTION('center_axis',(0.,-1.,0.));
#27064=DIRECTION('ref_axis',(0.245760053518537,0.,-0.969330694909929));
#27065=DIRECTION('',(0.,-1.,0.));
#27066=DIRECTION('center_axis',(0.,-1.,0.));
#27067=DIRECTION('ref_axis',(-0.245760053518569,0.,0.969330694909921));
#27068=DIRECTION('center_axis',(0.,1.,0.));
#27069=DIRECTION('ref_axis',(-0.245760053518569,0.,0.969330694909921));
#27070=DIRECTION('',(0.,-1.,0.));
#27071=DIRECTION('center_axis',(0.,-1.,0.));
#27072=DIRECTION('ref_axis',(0.711979844231348,0.,-0.702199901316075));
#27073=DIRECTION('center_axis',(0.,-1.,0.));
#27074=DIRECTION('ref_axis',(0.711979844231348,0.,-0.702199901316075));
#27075=DIRECTION('',(0.,-1.,0.));
#27076=DIRECTION('center_axis',(0.71197984423134,0.,-0.702199901316083));
#27077=DIRECTION('ref_axis',(0.702199901316083,0.,0.71197984423134));
#27078=DIRECTION('',(0.702199901316083,0.,0.71197984423134));
#27079=DIRECTION('',(0.,-1.,0.));
#27080=DIRECTION('center_axis',(0.,-1.,0.));
#27081=DIRECTION('ref_axis',(-0.711979844231334,0.,0.702199901316089));
#27082=DIRECTION('center_axis',(0.,1.,0.));
#27083=DIRECTION('ref_axis',(-0.711979844231334,0.,0.702199901316089));
#27084=DIRECTION('',(0.,-1.,0.));
#27085=DIRECTION('center_axis',(1.,0.,0.));
#27086=DIRECTION('ref_axis',(0.,0.,1.));
#27087=DIRECTION('',(0.,0.,1.));
#27088=DIRECTION('',(0.,-1.,0.));
#27089=DIRECTION('center_axis',(0.,-1.,0.));
#27090=DIRECTION('ref_axis',(-1.,0.,1.69176841847649E-14));
#27091=DIRECTION('center_axis',(0.,1.,0.));
#27092=DIRECTION('ref_axis',(-1.,0.,1.69176841847649E-14));
#27093=DIRECTION('',(0.,-1.,0.));
#27094=DIRECTION('center_axis',(0.709478283082607,0.,0.704727298913669));
#27095=DIRECTION('ref_axis',(-0.704727298913669,0.,0.709478283082607));
#27096=DIRECTION('',(-0.704727298913669,0.,0.709478283082607));
#27097=DIRECTION('',(0.,-1.,0.));
#27098=DIRECTION('center_axis',(0.,-1.,0.));
#27099=DIRECTION('ref_axis',(1.,0.,-4.03717463500059E-15));
#27100=DIRECTION('center_axis',(0.,-1.,0.));
#27101=DIRECTION('ref_axis',(1.,0.,-4.03717463500059E-15));
#27102=DIRECTION('',(0.,-1.,0.));
#27103=DIRECTION('center_axis',(1.,0.,0.));
#27104=DIRECTION('ref_axis',(0.,0.,1.));
#27105=DIRECTION('',(0.,0.,1.));
#27106=DIRECTION('',(0.,-1.,0.));
#27107=DIRECTION('center_axis',(0.707376432457449,0.,-0.706837027046385));
#27108=DIRECTION('ref_axis',(0.706837027046385,0.,0.707376432457449));
#27109=DIRECTION('',(0.706837027046385,0.,0.707376432457449));
#27110=DIRECTION('',(0.,-1.,0.));
#27111=DIRECTION('center_axis',(0.,0.,-1.));
#27112=DIRECTION('ref_axis',(1.,0.,0.));
#27113=DIRECTION('',(-1.,0.,-2.53764096072769E-16));
#27114=DIRECTION('center_axis',(0.,0.,1.));
#27115=DIRECTION('ref_axis',(-1.,0.,0.));
#27116=DIRECTION('',(-1.,0.,0.));
#27117=DIRECTION('center_axis',(0.,-1.,0.));
#27118=DIRECTION('ref_axis',(-1.,0.,0.));
#48123=CARTESIAN_POINT('',(0.,0.,0.));
#48124=CARTESIAN_POINT('Origin',(7.41771637130031,255.,47.007169160326));
#48125=CARTESIAN_POINT('',(7.90559015802673,15.,47.5000804575095));
#48126=CARTESIAN_POINT('',(7.90559015802673,495.,47.5000804575095));
#48127=CARTESIAN_POINT('',(7.90559015802673,255.,47.5000804575095));
#48128=CARTESIAN_POINT('',(7.41771637130031,495.,47.007169160326));
#48129=CARTESIAN_POINT('',(7.90559015802673,495.,47.5000804575095));
#48130=CARTESIAN_POINT('',(7.41771637130031,15.,47.007169160326));
#48131=CARTESIAN_POINT('',(7.41771637130031,255.,47.007169160326));
#48132=CARTESIAN_POINT('',(7.90559015802673,15.,47.5000804575095));
#48133=CARTESIAN_POINT('Origin',(7.73754453375374,255.,46.690609613792));
#48134=CARTESIAN_POINT('',(7.30402291514177,495.,46.8112703207193));
#48135=CARTESIAN_POINT('Origin',(7.73754453375374,495.,46.690609613792));
#48136=CARTESIAN_POINT('',(7.30402291514177,15.,46.8112703207193));
#48137=CARTESIAN_POINT('',(7.30402291514177,255.,46.8112703207193));
#48138=CARTESIAN_POINT('Origin',(7.73754453375374,15.,46.690609613792));
#48139=CARTESIAN_POINT('Origin',(4.92693912780791,255.,47.4728765656934));
#48140=CARTESIAN_POINT('',(5.65517411340273,495.,45.1153516005764));
#48141=CARTESIAN_POINT('Origin',(4.92693912780791,495.,47.4728765656934));
#48142=CARTESIAN_POINT('',(5.65517411340273,15.,45.1153516005764));
#48143=CARTESIAN_POINT('',(5.65517411340273,255.,45.1153516005764));
#48144=CARTESIAN_POINT('Origin',(4.92693912780791,15.,47.4728765656934));
#48145=CARTESIAN_POINT('Origin',(5.86914924474375,255.,44.4226470147914));
#48146=CARTESIAN_POINT('',(5.14414924474374,495.,44.4226470147914));
#48147=CARTESIAN_POINT('Origin',(5.86914924474375,495.,44.4226470147914));
#48148=CARTESIAN_POINT('',(5.14414924474374,15.,44.4226470147914));
#48149=CARTESIAN_POINT('',(5.14414924474374,255.,44.4226470147914));
#48150=CARTESIAN_POINT('Origin',(5.86914924474375,15.,44.4226470147914));
#48151=CARTESIAN_POINT('Origin',(5.14414924474375,255.,43.5036225521864));
#48152=CARTESIAN_POINT('',(5.14414924474375,495.,43.5036225521864));
#48153=CARTESIAN_POINT('',(5.14414924474374,495.,44.4226470147914));
#48154=CARTESIAN_POINT('',(5.14414924474375,15.,43.5036225521864));
#48155=CARTESIAN_POINT('',(5.14414924474375,255.,43.5036225521864));
#48156=CARTESIAN_POINT('',(5.14414924474374,15.,44.4226470147914));
#48157=CARTESIAN_POINT('Origin',(5.74414924474373,255.,43.5036225521863));
#48158=CARTESIAN_POINT('',(5.59669321263261,495.,42.9220241352404));
#48159=CARTESIAN_POINT('Origin',(5.74414924474373,495.,43.5036225521863));
#48160=CARTESIAN_POINT('',(5.59669321263261,15.,42.9220241352404));
#48161=CARTESIAN_POINT('',(5.59669321263261,255.,42.9220241352404));
#48162=CARTESIAN_POINT('Origin',(5.74414924474373,15.,43.5036225521863));
#48163=CARTESIAN_POINT('Origin',(5.01571081212747,255.,40.6305041508116));
#48164=CARTESIAN_POINT('',(7.26563149638805,495.,41.3560806824536));
#48165=CARTESIAN_POINT('Origin',(5.01571081212747,495.,40.6305041508116));
#48166=CARTESIAN_POINT('',(7.26563149638805,15.,41.3560806824536));
#48167=CARTESIAN_POINT('',(7.26563149638805,255.,41.3560806824536));
#48168=CARTESIAN_POINT('Origin',(5.01571081212747,15.,40.6305041508116));
#48169=CARTESIAN_POINT('Origin',(8.59805891280186,255.,41.7857749691141));
#48170=CARTESIAN_POINT('',(7.60128713087801,495.,40.8026951072716));
#48171=CARTESIAN_POINT('Origin',(8.59805891280186,495.,41.7857749691141));
#48172=CARTESIAN_POINT('',(7.60128713087801,15.,40.8026951072716));
#48173=CARTESIAN_POINT('',(7.60128713087801,255.,40.8026951072716));
#48174=CARTESIAN_POINT('Origin',(8.59805891280186,15.,41.7857749691141));
#48175=CARTESIAN_POINT('Origin',(8.23905763252352,255.,40.1560420081102));
#48176=CARTESIAN_POINT('',(8.23905763252352,495.,40.1560420081102));
#48177=CARTESIAN_POINT('',(8.23905763252352,495.,40.1560420081102));
#48178=CARTESIAN_POINT('',(8.23905763252352,15.,40.1560420081102));
#48179=CARTESIAN_POINT('',(8.23905763252352,255.,40.1560420081102));
#48180=CARTESIAN_POINT('',(8.23905763252352,15.,40.1560420081102));
#48181=CARTESIAN_POINT('Origin',(7.49147879608061,255.,39.4187321117283));
#48182=CARTESIAN_POINT('',(8.54147879608062,495.,39.4187321117283));
#48183=CARTESIAN_POINT('Origin',(7.49147879608061,495.,39.4187321117283));
#48184=CARTESIAN_POINT('',(8.54147879608062,15.,39.4187321117283));
#48185=CARTESIAN_POINT('',(8.54147879608062,255.,39.4187321117283));
#48186=CARTESIAN_POINT('Origin',(7.49147879608061,15.,39.4187321117283));
#48187=CARTESIAN_POINT('Origin',(8.54147879608062,255.,37.9151793916432));
#48188=CARTESIAN_POINT('',(8.54147879608062,495.,37.9151793916432));
#48189=CARTESIAN_POINT('',(8.54147879608062,495.,39.4187321117283));
#48190=CARTESIAN_POINT('',(8.54147879608062,15.,37.9151793916432));
#48191=CARTESIAN_POINT('',(8.54147879608062,255.,37.9151793916432));
#48192=CARTESIAN_POINT('',(8.54147879608062,15.,39.4187321117283));
#48193=CARTESIAN_POINT('Origin',(7.49147879608066,255.,37.9151793916432));
#48194=CARTESIAN_POINT('',(8.23643099331736,495.,37.1752157277839));
#48195=CARTESIAN_POINT('Origin',(7.49147879608066,495.,37.9151793916432));
#48196=CARTESIAN_POINT('',(8.23643099331736,15.,37.1752157277839));
#48197=CARTESIAN_POINT('',(8.23643099331736,255.,37.1752157277839));
#48198=CARTESIAN_POINT('Origin',(7.49147879608066,15.,37.9151793916432));
#48199=CARTESIAN_POINT('Origin',(5.4553112552519,255.,34.375346814161));
#48200=CARTESIAN_POINT('',(5.4553112552519,495.,34.375346814161));
#48201=CARTESIAN_POINT('',(5.4553112552519,495.,34.375346814161));
#48202=CARTESIAN_POINT('',(5.4553112552519,15.,34.375346814161));
#48203=CARTESIAN_POINT('',(5.4553112552519,255.,34.375346814161));
#48204=CARTESIAN_POINT('',(5.4553112552519,15.,34.375346814161));
#48205=CARTESIAN_POINT('Origin',(6.23573736664277,255.,33.6001467853559));
#48206=CARTESIAN_POINT('',(5.13573736664277,495.,33.6001467853559));
#48207=CARTESIAN_POINT('Origin',(6.23573736664277,495.,33.6001467853559));
#48208=CARTESIAN_POINT('',(5.13573736664277,15.,33.6001467853559));
#48209=CARTESIAN_POINT('',(5.13573736664277,255.,33.6001467853559));
#48210=CARTESIAN_POINT('Origin',(6.23573736664277,15.,33.6001467853559));
#48211=CARTESIAN_POINT('Origin',(5.13573736664277,255.,31.0022770426652));
#48212=CARTESIAN_POINT('',(5.13573736664277,495.,31.0022770426652));
#48213=CARTESIAN_POINT('',(5.13573736664277,495.,31.0022770426652));
#48214=CARTESIAN_POINT('',(5.13573736664277,15.,31.0022770426652));
#48215=CARTESIAN_POINT('',(5.13573736664277,255.,31.0022770426652));
#48216=CARTESIAN_POINT('',(5.13573736664277,15.,31.0022770426652));
#48217=CARTESIAN_POINT('Origin',(6.13725012930742,255.,30.));
#48218=CARTESIAN_POINT('',(6.13725012930742,495.,30.));
#48219=CARTESIAN_POINT('',(6.13725012930742,495.,30.));
#48220=CARTESIAN_POINT('',(6.13725012930742,15.,30.));
#48221=CARTESIAN_POINT('',(6.13725012930742,255.,30.));
#48222=CARTESIAN_POINT('',(6.13725012930742,15.,30.));
#48223=CARTESIAN_POINT('Origin',(20.1330790931884,495.,38.7500402287547));
#48224=CARTESIAN_POINT('',(22.362340210653,495.,47.5000804575095));
#48225=CARTESIAN_POINT('',(5.13573736664277,495.,47.5000804575095));
#48226=CARTESIAN_POINT('',(22.8502139973794,495.,47.007169160326));
#48227=CARTESIAN_POINT('',(22.362340210653,495.,47.5000804575095));
#48228=CARTESIAN_POINT('',(22.963907453538,495.,46.8112703207193));
#48229=CARTESIAN_POINT('Origin',(22.530385834926,495.,46.690609613792));
#48230=CARTESIAN_POINT('',(24.612756255277,495.,45.1153516005764));
#48231=CARTESIAN_POINT('Origin',(25.3409912408718,495.,47.4728765656934));
#48232=CARTESIAN_POINT('',(25.123781123936,495.,44.4226470147914));
#48233=CARTESIAN_POINT('Origin',(24.398781123936,495.,44.4226470147914));
#48234=CARTESIAN_POINT('',(25.123781123936,495.,43.5036225521864));
#48235=CARTESIAN_POINT('',(25.123781123936,495.,44.4226470147914));
#48236=CARTESIAN_POINT('',(24.6712371560471,495.,42.9220241352404));
#48237=CARTESIAN_POINT('Origin',(24.523781123936,495.,43.5036225521863));
#48238=CARTESIAN_POINT('',(23.0022988722917,495.,41.3560806824536));
#48239=CARTESIAN_POINT('Origin',(25.2522195565523,495.,40.6305041508116));
#48240=CARTESIAN_POINT('',(22.6666432378017,495.,40.8026951072716));
#48241=CARTESIAN_POINT('Origin',(21.6698714558779,495.,41.7857749691141));
#48242=CARTESIAN_POINT('',(22.0288727361562,495.,40.1560420081102));
#48243=CARTESIAN_POINT('',(22.0288727361562,495.,40.1560420081102));
#48244=CARTESIAN_POINT('',(21.7264515725991,495.,39.4187321117283));
#48245=CARTESIAN_POINT('Origin',(22.7764515725991,495.,39.4187321117283));
#48246=CARTESIAN_POINT('',(21.7264515725991,495.,37.9151793916432));
#48247=CARTESIAN_POINT('',(21.7264515725991,495.,39.4187321117283));
#48248=CARTESIAN_POINT('',(22.0314993753624,495.,37.1752157277839));
#48249=CARTESIAN_POINT('Origin',(22.7764515725991,495.,37.9151793916432));
#48250=CARTESIAN_POINT('',(24.8126191134278,495.,34.375346814161));
#48251=CARTESIAN_POINT('',(24.8126191134278,495.,34.375346814161));
#48252=CARTESIAN_POINT('',(25.132193002037,495.,33.6001467853559));
#48253=CARTESIAN_POINT('Origin',(24.032193002037,495.,33.6001467853559));
#48254=CARTESIAN_POINT('',(25.132193002037,495.,31.0022770426652));
#48255=CARTESIAN_POINT('',(25.132193002037,495.,31.0022770426652));
#48256=CARTESIAN_POINT('',(24.1306802393723,495.,30.));
#48257=CARTESIAN_POINT('',(24.1306802393723,495.,30.));
#48258=CARTESIAN_POINT('',(5.13573736664278,495.,30.));
#48259=CARTESIAN_POINT('Origin',(22.8502139973794,255.,47.007169160326));
#48260=CARTESIAN_POINT('',(22.362340210653,15.,47.5000804575095));
#48261=CARTESIAN_POINT('',(22.362340210653,255.,47.5000804575095));
#48262=CARTESIAN_POINT('',(22.8502139973794,15.,47.007169160326));
#48263=CARTESIAN_POINT('',(22.362340210653,15.,47.5000804575095));
#48264=CARTESIAN_POINT('',(22.8502139973794,255.,47.007169160326));
#48265=CARTESIAN_POINT('Origin',(22.530385834926,255.,46.690609613792));
#48266=CARTESIAN_POINT('',(22.963907453538,15.,46.8112703207193));
#48267=CARTESIAN_POINT('Origin',(22.530385834926,15.,46.690609613792));
#48268=CARTESIAN_POINT('',(22.963907453538,255.,46.8112703207193));
#48269=CARTESIAN_POINT('Origin',(25.3409912408718,255.,47.4728765656934));
#48270=CARTESIAN_POINT('',(24.612756255277,15.,45.1153516005764));
#48271=CARTESIAN_POINT('Origin',(25.3409912408718,15.,47.4728765656934));
#48272=CARTESIAN_POINT('',(24.612756255277,255.,45.1153516005764));
#48273=CARTESIAN_POINT('Origin',(24.398781123936,255.,44.4226470147914));
#48274=CARTESIAN_POINT('',(25.123781123936,15.,44.4226470147914));
#48275=CARTESIAN_POINT('Origin',(24.398781123936,15.,44.4226470147914));
#48276=CARTESIAN_POINT('',(25.123781123936,255.,44.4226470147914));
#48277=CARTESIAN_POINT('Origin',(25.123781123936,255.,43.5036225521864));
#48278=CARTESIAN_POINT('',(25.123781123936,15.,43.5036225521864));
#48279=CARTESIAN_POINT('',(25.123781123936,15.,44.4226470147914));
#48280=CARTESIAN_POINT('',(25.123781123936,255.,43.5036225521864));
#48281=CARTESIAN_POINT('Origin',(24.523781123936,255.,43.5036225521863));
#48282=CARTESIAN_POINT('',(24.6712371560471,15.,42.9220241352404));
#48283=CARTESIAN_POINT('Origin',(24.523781123936,15.,43.5036225521863));
#48284=CARTESIAN_POINT('',(24.6712371560471,255.,42.9220241352404));
#48285=CARTESIAN_POINT('Origin',(25.2522195565523,255.,40.6305041508116));
#48286=CARTESIAN_POINT('',(23.0022988722917,15.,41.3560806824536));
#48287=CARTESIAN_POINT('Origin',(25.2522195565523,15.,40.6305041508116));
#48288=CARTESIAN_POINT('',(23.0022988722917,255.,41.3560806824536));
#48289=CARTESIAN_POINT('Origin',(21.6698714558779,255.,41.7857749691141));
#48290=CARTESIAN_POINT('',(22.6666432378017,15.,40.8026951072716));
#48291=CARTESIAN_POINT('Origin',(21.6698714558779,15.,41.7857749691141));
#48292=CARTESIAN_POINT('',(22.6666432378017,255.,40.8026951072716));
#48293=CARTESIAN_POINT('Origin',(22.0288727361562,255.,40.1560420081102));
#48294=CARTESIAN_POINT('',(22.0288727361562,15.,40.1560420081102));
#48295=CARTESIAN_POINT('',(22.0288727361562,15.,40.1560420081102));
#48296=CARTESIAN_POINT('',(22.0288727361562,255.,40.1560420081102));
#48297=CARTESIAN_POINT('Origin',(22.7764515725991,255.,39.4187321117283));
#48298=CARTESIAN_POINT('',(21.7264515725991,15.,39.4187321117283));
#48299=CARTESIAN_POINT('Origin',(22.7764515725991,15.,39.4187321117283));
#48300=CARTESIAN_POINT('',(21.7264515725991,255.,39.4187321117283));
#48301=CARTESIAN_POINT('Origin',(21.7264515725991,255.,37.9151793916432));
#48302=CARTESIAN_POINT('',(21.7264515725991,15.,37.9151793916432));
#48303=CARTESIAN_POINT('',(21.7264515725991,15.,39.4187321117283));
#48304=CARTESIAN_POINT('',(21.7264515725991,255.,37.9151793916432));
#48305=CARTESIAN_POINT('Origin',(22.7764515725991,255.,37.9151793916432));
#48306=CARTESIAN_POINT('',(22.0314993753624,15.,37.1752157277839));
#48307=CARTESIAN_POINT('Origin',(22.7764515725991,15.,37.9151793916432));
#48308=CARTESIAN_POINT('',(22.0314993753624,255.,37.1752157277839));
#48309=CARTESIAN_POINT('Origin',(24.8126191134278,255.,34.375346814161));
#48310=CARTESIAN_POINT('',(24.8126191134278,15.,34.375346814161));
#48311=CARTESIAN_POINT('',(24.8126191134278,15.,34.375346814161));
#48312=CARTESIAN_POINT('',(24.8126191134278,255.,34.375346814161));
#48313=CARTESIAN_POINT('Origin',(24.032193002037,255.,33.6001467853559));
#48314=CARTESIAN_POINT('',(25.132193002037,15.,33.6001467853559));
#48315=CARTESIAN_POINT('Origin',(24.032193002037,15.,33.6001467853559));
#48316=CARTESIAN_POINT('',(25.132193002037,255.,33.6001467853559));
#48317=CARTESIAN_POINT('Origin',(25.132193002037,255.,31.0022770426652));
#48318=CARTESIAN_POINT('',(25.132193002037,15.,31.0022770426652));
#48319=CARTESIAN_POINT('',(25.132193002037,15.,31.0022770426652));
#48320=CARTESIAN_POINT('',(25.132193002037,255.,31.0022770426652));
#48321=CARTESIAN_POINT('Origin',(24.1306802393723,255.,30.));
#48322=CARTESIAN_POINT('',(24.1306802393723,15.,30.));
#48323=CARTESIAN_POINT('',(24.1306802393723,15.,30.));
#48324=CARTESIAN_POINT('',(24.1306802393723,255.,30.));
#48325=CARTESIAN_POINT('Origin',(15.1339651843399,255.,30.));
#48326=CARTESIAN_POINT('',(25.132193002037,15.,30.));
#48327=CARTESIAN_POINT('Origin',(22.362340210653,255.,47.5000804575095));
#48328=CARTESIAN_POINT('',(25.132193002037,15.,47.5000804575095));
#48329=CARTESIAN_POINT('Origin',(20.1330790931884,15.,38.7500402287547));
#48355=UNCERTAINTY_MEASURE_WITH_UNIT(LENGTH_MEASURE(0.01),#48370,
'DISTANCE_ACCURACY_VALUE',
'Maximum model space distance between geometric entities at asserted c
onnectivities');
#48356=UNCERTAINTY_MEASURE_WITH_UNIT(LENGTH_MEASURE(0.01),#48370,
'DISTANCE_ACCURACY_VALUE',
'Maximum model space distance between geometric entities at asserted c
onnectivities');
#48368=(
GEOMETRIC_REPRESENTATION_CONTEXT(3)
GLOBAL_UNCERTAINTY_ASSIGNED_CONTEXT((#48355))
GLOBAL_UNIT_ASSIGNED_CONTEXT((#48370,#48372,#48373))
REPRESENTATION_CONTEXT('','3D')
);
#48369=(
GEOMETRIC_REPRESENTATION_CONTEXT(3)
GLOBAL_UNCERTAINTY_ASSIGNED_CONTEXT((#48356))
GLOBAL_UNIT_ASSIGNED_CONTEXT((#48370,#48372,#48373))
REPRESENTATION_CONTEXT('','3D')
);
#48370=(
LENGTH_UNIT()
NAMED_UNIT(*)
SI_UNIT(.MILLI.,.METRE.)
);
#48372=(
NAMED_UNIT(*)
PLANE_ANGLE_UNIT()
SI_UNIT($,.RADIAN.)
);
#48373=(
NAMED_UNIT(*)
SI_UNIT($,.STERADIAN.)
SOLID_ANGLE_UNIT()
);
#48385=SHAPE_DEFINITION_REPRESENTATION(#48397,#48423);
#48397=PRODUCT_DEFINITION_SHAPE('',$,#48436);
#48423=SHAPE_REPRESENTATION('',(#21839),#48368);
#48424=PRODUCT_DEFINITION_CONTEXT('part definition',#48462,'design');
#48436=PRODUCT_DEFINITION('Rail_01','Rail_01',#48448,#48424);
#48448=PRODUCT_DEFINITION_FORMATION('',$,#48475);
#48462=APPLICATION_CONTEXT(
'Core Data for Automotive Mechanical Design Process');
#48463=PRODUCT_CONTEXT('part definition',#48462,'mechanical');
#48475=PRODUCT('Rail_01','Rail_01',$,(#48463));
#48504=COLOUR_RGB('Sky Blue',0.24,0.69,0.87);
#48505=FILL_AREA_STYLE_COLOUR('',#48504);
#48506=FILL_AREA_STYLE('',(#48505));
#48507=SURFACE_STYLE_FILL_AREA(#48506);
#48508=SURFACE_SIDE_STYLE('',(#48507));
#48509=SURFACE_STYLE_USAGE(.BOTH.,#48508);
#48510=PRESENTATION_STYLE_ASSIGNMENT((#48509));
ENDSEC;
END-ISO-10303-21;
